ISO-10303-21;
HEADER;
FILE_DESCRIPTION((''),'2;1');
FILE_NAME('Spring_Washer_3.step','2026-10-09T11:34:15-07:00',(''),(''),'','','');
FILE_SCHEMA (('AUTOMOTIVE_DESIGN { 1 0 10303 214 3 1 1 }'));
ENDSEC;
DATA;
#10=MECHANICAL_DESIGN_GEOMETRIC_PRESENTATION_REPRESENTATION('',(#636),#117170);
#594=SHAPE_REPRESENTATION_RELATIONSHIP('SRR','None',#117249,#615) ;
#615=ADVANCED_BREP_SHAPE_REPRESENTATION('',(#657),#117157) ;
#636=STYLED_ITEM('',(#117355),#657) ;
#657=MANIFOLD_SOLID_BREP('Body1',#49065) ;
#731=FACE_BOUND('',#15267,.T.) ;
#732=FACE_BOUND('',#15270,.T.) ;
#2484=PLANE('',#52012) ;
#2485=PLANE('',#52016) ;
#4269=LINE('',#87521,#7483) ;
#4270=LINE('',#87529,#7484) ;
#7483=VECTOR('',#61736,2.5) ;
#7484=VECTOR('',#61747,3.) ;
#9991=CYLINDRICAL_SURFACE('',#52010,2.5) ;
#9992=CYLINDRICAL_SURFACE('',#52014,3.) ;
#12111=FACE_OUTER_BOUND('',#15264,.T.) ;
#12112=FACE_OUTER_BOUND('',#15265,.T.) ;
#12113=FACE_OUTER_BOUND('',#15266,.T.) ;
#12114=FACE_OUTER_BOUND('',#15268,.T.) ;
#12115=FACE_OUTER_BOUND('',#15269,.T.) ;
#15264=EDGE_LOOP('',(#37310,#37311,#37312,#37313)) ;
#15265=EDGE_LOOP('',(#37314,#37315,#37316,#37317)) ;
#15266=EDGE_LOOP('',(#37318)) ;
#15267=EDGE_LOOP('',(#37319)) ;
#15268=EDGE_LOOP('',(#37320,#37321,#37322,#37323)) ;
#15269=EDGE_LOOP('',(#37324)) ;
#15270=EDGE_LOOP('',(#37325)) ;
#18400=CIRCLE('',#52007,2.5) ;
#18401=CIRCLE('',#52008,0.45) ;
#18402=CIRCLE('',#52009,2.95) ;
#18403=CIRCLE('',#52011,2.5) ;
#18404=CIRCLE('',#52013,3.) ;
#18405=CIRCLE('',#52015,3.) ;
#21388=VERTEX_POINT('',#87514) ;
#21389=VERTEX_POINT('',#87516) ;
#21390=VERTEX_POINT('',#87520) ;
#21391=VERTEX_POINT('',#87524) ;
#21392=VERTEX_POINT('',#87527) ;
#26933=EDGE_CURVE('',#21388,#21388,#18400,.T.) ;
#26934=EDGE_CURVE('',#21388,#21389,#18401,.T.) ;
#26935=EDGE_CURVE('',#21389,#21389,#18402,.T.) ;
#26936=EDGE_CURVE('',#21388,#21390,#4269,.T.) ;
#26937=EDGE_CURVE('',#21390,#21390,#18403,.T.) ;
#26938=EDGE_CURVE('',#21391,#21391,#18404,.T.) ;
#26939=EDGE_CURVE('',#21392,#21392,#18405,.T.) ;
#26940=EDGE_CURVE('',#21392,#21391,#4270,.T.) ;
#37310=ORIENTED_EDGE('',*,*,#26933,.T.) ;
#37311=ORIENTED_EDGE('',*,*,#26934,.T.) ;
#37312=ORIENTED_EDGE('',*,*,#26935,.T.) ;
#37313=ORIENTED_EDGE('',*,*,#26934,.F.) ;
#37314=ORIENTED_EDGE('',*,*,#26933,.F.) ;
#37315=ORIENTED_EDGE('',*,*,#26936,.T.) ;
#37316=ORIENTED_EDGE('',*,*,#26937,.F.) ;
#37317=ORIENTED_EDGE('',*,*,#26936,.F.) ;
#37318=ORIENTED_EDGE('',*,*,#26938,.F.) ;
#37319=ORIENTED_EDGE('',*,*,#26935,.F.) ;
#37320=ORIENTED_EDGE('',*,*,#26939,.F.) ;
#37321=ORIENTED_EDGE('',*,*,#26940,.T.) ;
#37322=ORIENTED_EDGE('',*,*,#26938,.T.) ;
#37323=ORIENTED_EDGE('',*,*,#26940,.F.) ;
#37324=ORIENTED_EDGE('',*,*,#26939,.T.) ;
#37325=ORIENTED_EDGE('',*,*,#26937,.T.) ;
#45696=TOROIDAL_SURFACE('',#52006,2.95,0.45) ;
#47329=ADVANCED_FACE('',(#12111),#45696,.T.) ;
#47330=ADVANCED_FACE('',(#12112),#9991,.F.) ;
#47331=ADVANCED_FACE('',(#12113,#731),#2484,.F.) ;
#47332=ADVANCED_FACE('',(#12114),#9992,.T.) ;
#47333=ADVANCED_FACE('',(#12115,#732),#2485,.T.) ;
#49065=CLOSED_SHELL('',(#47329,#47330,#47331,#47332,#47333)) ;
#52005=AXIS2_PLACEMENT_3D('',#87512,#61724,#61725) ;
#52006=AXIS2_PLACEMENT_3D('',#87513,#61726,#61727) ;
#52007=AXIS2_PLACEMENT_3D('',#87515,#61728,#61729) ;
#52008=AXIS2_PLACEMENT_3D('',#87517,#61730,#61731) ;
#52009=AXIS2_PLACEMENT_3D('',#87518,#61732,#61733) ;
#52010=AXIS2_PLACEMENT_3D('',#87519,#61734,#61735) ;
#52011=AXIS2_PLACEMENT_3D('',#87522,#61737,#61738) ;
#52012=AXIS2_PLACEMENT_3D('',#87523,#61739,#61740) ;
#52013=AXIS2_PLACEMENT_3D('',#87525,#61741,#61742) ;
#52014=AXIS2_PLACEMENT_3D('',#87526,#61743,#61744) ;
#52015=AXIS2_PLACEMENT_3D('',#87528,#61745,#61746) ;
#52016=AXIS2_PLACEMENT_3D('',#87530,#61748,#61749) ;
#61724=DIRECTION('axis',(0.,0.,1.)) ;
#61725=DIRECTION('refdir',(1.,0.,0.)) ;
#61726=DIRECTION('center_axis',(-2.52374105052742E-18,-5.60383084497445E-34,
1.)) ;
#61727=DIRECTION('ref_axis',(1.,0.,0.)) ;
#61728=DIRECTION('center_axis',(2.52374105052742E-18,5.60383084497445E-34,
-1.)) ;
#61729=DIRECTION('ref_axis',(1.,1.0086895520954E-34,2.52374105052742E-18)) ;
#61730=DIRECTION('center_axis',(0.,-1.,-5.60383084497445E-34)) ;
#61731=DIRECTION('ref_axis',(-1.,0.,0.)) ;
#61732=DIRECTION('center_axis',(-2.52374105052742E-18,-5.60383084497445E-34,
1.)) ;
#61733=DIRECTION('ref_axis',(1.,1.0086895520954E-34,2.52374105052742E-18)) ;
#61734=DIRECTION('center_axis',(0.,0.,-1.)) ;
#61735=DIRECTION('ref_axis',(1.,0.,0.)) ;
#61736=DIRECTION('',(0.,0.,-1.)) ;
#61737=DIRECTION('center_axis',(-2.52374105052742E-18,-5.60383084497445E-34,
1.)) ;
#61738=DIRECTION('ref_axis',(1.,3.40207761657885E-68,2.52374105052742E-18)) ;
#61739=DIRECTION('center_axis',(2.52374105052742E-18,5.60383084497445E-34,
-1.)) ;
#61740=DIRECTION('ref_axis',(1.,3.40207761657885E-68,2.52374105052742E-18)) ;
#61741=DIRECTION('center_axis',(2.52374105052742E-18,5.60383084497445E-34,
-1.)) ;
#61742=DIRECTION('ref_axis',(1.,3.40207761657885E-68,2.52374105052742E-18)) ;
#61743=DIRECTION('center_axis',(0.,0.,-1.)) ;
#61744=DIRECTION('ref_axis',(1.,0.,0.)) ;
#61745=DIRECTION('center_axis',(2.52374105052742E-18,5.60383084497445E-34,
-1.)) ;
#61746=DIRECTION('ref_axis',(1.,3.40207761657885E-68,2.52374105052742E-18)) ;
#61747=DIRECTION('',(0.,0.,1.)) ;
#61748=DIRECTION('center_axis',(2.52374105052742E-18,5.60383084497445E-34,
-1.)) ;
#61749=DIRECTION('ref_axis',(1.,3.40207761657885E-68,2.52374105052742E-18)) ;
#87512=CARTESIAN_POINT('',(0.,0.,0.)) ;
#87513=CARTESIAN_POINT('Origin',(30.7,254.8,30.2713203435596)) ;
#87514=CARTESIAN_POINT('',(28.2,254.8,30.2713203435596)) ;
#87515=CARTESIAN_POINT('Origin',(30.7,254.8,30.2713203435596)) ;
#87516=CARTESIAN_POINT('',(27.75,254.8,30.7213203435596)) ;
#87517=CARTESIAN_POINT('Origin',(27.75,254.8,30.2713203435596)) ;
#87518=CARTESIAN_POINT('Origin',(30.7,254.8,30.7213203435596)) ;
#87519=CARTESIAN_POINT('Origin',(30.7,254.8,30.7213203435596)) ;
#87520=CARTESIAN_POINT('',(28.2,254.8,28.7213203435596)) ;
#87521=CARTESIAN_POINT('',(28.2,254.8,30.7213203435596)) ;
#87522=CARTESIAN_POINT('Origin',(30.7,254.8,28.7213203435596)) ;
#87523=CARTESIAN_POINT('Origin',(30.7,254.8,30.7213203435596)) ;
#87524=CARTESIAN_POINT('',(27.7,254.8,30.7213203435596)) ;
#87525=CARTESIAN_POINT('Origin',(30.7,254.8,30.7213203435596)) ;
#87526=CARTESIAN_POINT('Origin',(30.7,254.8,30.7213203435596)) ;
#87527=CARTESIAN_POINT('',(27.7,254.8,28.7213203435596)) ;
#87528=CARTESIAN_POINT('Origin',(30.7,254.8,28.7213203435596)) ;
#87529=CARTESIAN_POINT('',(27.7,254.8,30.7213203435596)) ;
#87530=CARTESIAN_POINT('Origin',(30.7,254.8,28.7213203435596)) ;
#117134=UNCERTAINTY_MEASURE_WITH_UNIT(LENGTH_MEASURE(0.01),#117171,
'DISTANCE_ACCURACY_VALUE',
'Maximum model space distance between geometric entities at asserted c
onnectivities') ;
#117147=UNCERTAINTY_MEASURE_WITH_UNIT(LENGTH_MEASURE(0.01),#117171,
'DISTANCE_ACCURACY_VALUE',
'Maximum model space distance between geometric entities at asserted c
onnectivities') ;
#117157=(
GEOMETRIC_REPRESENTATION_CONTEXT(3)
GLOBAL_UNCERTAINTY_ASSIGNED_CONTEXT((#117134))
GLOBAL_UNIT_ASSIGNED_CONTEXT((#117171,#117173,#117174))
REPRESENTATION_CONTEXT('','3D')
) ;
#117170=(
GEOMETRIC_REPRESENTATION_CONTEXT(3)
GLOBAL_UNCERTAINTY_ASSIGNED_CONTEXT((#117147))
GLOBAL_UNIT_ASSIGNED_CONTEXT((#117171,#117173,#117174))
REPRESENTATION_CONTEXT('','3D')
) ;
#117171=(
LENGTH_UNIT()
NAMED_UNIT(*)
SI_UNIT(.MILLI.,.METRE.)
) ;
#117173=(
NAMED_UNIT(*)
PLANE_ANGLE_UNIT()
SI_UNIT($,.RADIAN.)
) ;
#117174=(
NAMED_UNIT(*)
SI_UNIT($,.STERADIAN.)
SOLID_ANGLE_UNIT()
) ;
#117184=SHAPE_DEFINITION_REPRESENTATION(#117206,#117249) ;
#117206=PRODUCT_DEFINITION_SHAPE('',$,#117272) ;
#117249=SHAPE_REPRESENTATION('',(#52005),#117157) ;
#117262=PRODUCT_DEFINITION_CONTEXT('part definition',#117330,'design') ;
#117272=PRODUCT_DEFINITION('Spring_Washer_3','Spring_Washer_3',#117294,
#117262) ;
#117294=PRODUCT_DEFINITION_FORMATION('',$,#117341) ;
#117330=APPLICATION_CONTEXT(
'Core Data for Automotive Mechanical Design Process') ;
#117331=PRODUCT_CONTEXT('part definition',#117330,'mechanical') ;
#117341=PRODUCT('Spring_Washer_3','Spring_Washer_3',$,(#117331)) ;
#117355=PRESENTATION_STYLE_ASSIGNMENT((#117357)) ;
#117357=SURFACE_STYLE_USAGE(.BOTH.,#117359) ;
#117359=SURFACE_SIDE_STYLE('',(#117361)) ;
#117361=SURFACE_STYLE_FILL_AREA(#117363) ;
#117363=FILL_AREA_STYLE('Opaque(160,160,160)',(#117365)) ;
#117365=FILL_AREA_STYLE_COLOUR('Opaque(160,160,160)',#117367) ;
#117367=COLOUR_RGB('Opaque(160,160,160)', 0.09019608, 0.27058824, 0.51372549) ;
ENDSEC;
END-ISO-10303-21;
